ISO-10303-21;
HEADER;
/* Generated by software containing ST-Developer
 * from STEP Tools, Inc. (www.steptools.com) 
 */

FILE_DESCRIPTION(
/* description */ ('STEP AP214'),
/* implementation_level */ '2;1');

FILE_NAME(
/* name */ 'Coupling Clamp Screw 2.step',
/* time_stamp */ '2026-11-15T14:49:54-08:00',
/* author */ (''),
/* organization */ (''),
/* preprocessor_version */ 'ST-DEVELOPER v20.2',
/* originating_system */ 'Autodesk Translation Framework v15.17.0.0',
/* authorisation */ '');

FILE_SCHEMA (('AUTOMOTIVE_DESIGN { 1 0 10303 214 3 1 1 }'));
ENDSEC;

DATA;
#10=MECHANICAL_DESIGN_GEOMETRIC_PRESENTATION_REPRESENTATION('',(#1118),#66721);
#79=TOROIDAL_SURFACE('',#27985,4.3999999999,0.6);
#552=CONICAL_SURFACE('',#27998,2.693275,0.785398163397448);
#1056=SHAPE_REPRESENTATION_RELATIONSHIP('SRR','None',#66919,#1087);
#1087=ADVANCED_BREP_SHAPE_REPRESENTATION('',(#1153),#66710);
#1118=STYLED_ITEM('',(#67095),#1153);
#1153=MANIFOLD_SOLID_BREP('Body1',#25684);
#1406=FACE_BOUND('',#5020,.T.);
#1407=FACE_BOUND('',#5024,.T.);
#2045=PLANE('',#27980);
#2046=PLANE('',#27988);
#2047=PLANE('',#27989);
#2048=PLANE('',#27990);
#2049=PLANE('',#27991);
#2050=PLANE('',#27992);
#2051=PLANE('',#27993);
#2052=PLANE('',#27994);
#2053=PLANE('',#27995);
#2054=PLANE('',#27996);
#3339=FACE_OUTER_BOUND('',#5019,.T.);
#3340=FACE_OUTER_BOUND('',#5021,.T.);
#3341=FACE_OUTER_BOUND('',#5022,.T.);
#3342=FACE_OUTER_BOUND('',#5023,.T.);
#3343=FACE_OUTER_BOUND('',#5025,.T.);
#3344=FACE_OUTER_BOUND('',#5026,.T.);
#3345=FACE_OUTER_BOUND('',#5027,.T.);
#3346=FACE_OUTER_BOUND('',#5028,.T.);
#3347=FACE_OUTER_BOUND('',#5029,.T.);
#3348=FACE_OUTER_BOUND('',#5030,.T.);
#3349=FACE_OUTER_BOUND('',#5031,.T.);
#3350=FACE_OUTER_BOUND('',#5032,.T.);
#3351=FACE_OUTER_BOUND('',#5033,.T.);
#3352=FACE_OUTER_BOUND('',#5034,.T.);
#5019=EDGE_LOOP('',(#22024));
#5020=EDGE_LOOP('',(#22025));
#5021=EDGE_LOOP('',(#22026,#22027,#22028,#22029));
#5022=EDGE_LOOP('',(#22030,#22031,#22032,#22033));
#5023=EDGE_LOOP('',(#22034));
#5024=EDGE_LOOP('',(#22035,#22036,#22037,#22038,#22039,#22040));
#5025=EDGE_LOOP('',(#22041,#22042,#22043,#22044,#22045,#22046));
#5026=EDGE_LOOP('',(#22047,#22048,#22049,#22050));
#5027=EDGE_LOOP('',(#22051,#22052,#22053,#22054));
#5028=EDGE_LOOP('',(#22055,#22056,#22057,#22058));
#5029=EDGE_LOOP('',(#22059,#22060,#22061,#22062));
#5030=EDGE_LOOP('',(#22063,#22064,#22065,#22066));
#5031=EDGE_LOOP('',(#22067,#22068,#22069,#22070));
#5032=EDGE_LOOP('',(#22071));
#5033=EDGE_LOOP('',(#22072,#22073,#22074,#22075));
#5034=EDGE_LOOP('',(#22076,#22077,#22078,#22079));
#6941=LINE('',#64130,#8930);
#6942=LINE('',#64139,#8931);
#6943=LINE('',#64141,#8932);
#6944=LINE('',#64143,#8933);
#6945=LINE('',#64145,#8934);
#6946=LINE('',#64147,#8935);
#6947=LINE('',#64148,#8936);
#6948=LINE('',#64152,#8937);
#6949=LINE('',#64154,#8938);
#6950=LINE('',#64156,#8939);
#6951=LINE('',#64158,#8940);
#6952=LINE('',#64160,#8941);
#6953=LINE('',#64161,#8942);
#6954=LINE('',#64163,#8943);
#6955=LINE('',#64164,#8944);
#6956=LINE('',#64166,#8945);
#6957=LINE('',#64168,#8946);
#6958=LINE('',#64170,#8947);
#6959=LINE('',#64172,#8948);
#6960=LINE('',#64180,#8949);
#6961=LINE('',#64182,#8950);
#8930=VECTOR('',#34100,5.);
#8931=VECTOR('',#34111,1000.);
#8932=VECTOR('',#34112,1000.);
#8933=VECTOR('',#34113,1000.);
#8934=VECTOR('',#34114,1000.);
#8935=VECTOR('',#34115,1000.);
#8936=VECTOR('',#34116,1000.);
#8937=VECTOR('',#34119,1000.);
#8938=VECTOR('',#34120,1000.);
#8939=VECTOR('',#34121,1000.);
#8940=VECTOR('',#34122,1000.);
#8941=VECTOR('',#34123,1000.);
#8942=VECTOR('',#34124,1000.);
#8943=VECTOR('',#34127,1000.);
#8944=VECTOR('',#34128,1000.);
#8945=VECTOR('',#34131,1000.);
#8946=VECTOR('',#34134,1000.);
#8947=VECTOR('',#34137,1000.);
#8948=VECTOR('',#34140,1000.);
#8949=VECTOR('',#34151,2.693275);
#8950=VECTOR('',#34154,3.);
#10350=CIRCLE('',#27981,5.);
#10351=CIRCLE('',#27982,3.);
#10352=CIRCLE('',#27984,5.);
#10353=CIRCLE('',#27986,0.6);
#10354=CIRCLE('',#27987,4.4);
#10355=CIRCLE('',#27997,2.38655);
#10356=CIRCLE('',#27999,3.);
#12393=VERTEX_POINT('',#64124);
#12394=VERTEX_POINT('',#64126);
#12395=VERTEX_POINT('',#64129);
#12396=VERTEX_POINT('',#64133);
#12397=VERTEX_POINT('',#64137);
#12398=VERTEX_POINT('',#64138);
#12399=VERTEX_POINT('',#64140);
#12400=VERTEX_POINT('',#64142);
#12401=VERTEX_POINT('',#64144);
#12402=VERTEX_POINT('',#64146);
#12403=VERTEX_POINT('',#64150);
#12404=VERTEX_POINT('',#64151);
#12405=VERTEX_POINT('',#64153);
#12406=VERTEX_POINT('',#64155);
#12407=VERTEX_POINT('',#64157);
#12408=VERTEX_POINT('',#64159);
#12409=VERTEX_POINT('',#64175);
#12410=VERTEX_POINT('',#64178);
#15705=EDGE_CURVE('',#12393,#12393,#10350,.T.);
#15706=EDGE_CURVE('',#12394,#12394,#10351,.T.);
#15707=EDGE_CURVE('',#12393,#12395,#6941,.T.);
#15708=EDGE_CURVE('',#12395,#12395,#10352,.T.);
#15709=EDGE_CURVE('',#12395,#12396,#10353,.T.);
#15710=EDGE_CURVE('',#12396,#12396,#10354,.T.);
#15711=EDGE_CURVE('',#12397,#12398,#6942,.T.);
#15712=EDGE_CURVE('',#12398,#12399,#6943,.T.);
#15713=EDGE_CURVE('',#12399,#12400,#6944,.T.);
#15714=EDGE_CURVE('',#12400,#12401,#6945,.T.);
#15715=EDGE_CURVE('',#12401,#12402,#6946,.T.);
#15716=EDGE_CURVE('',#12402,#12397,#6947,.T.);
#15717=EDGE_CURVE('',#12403,#12404,#6948,.T.);
#15718=EDGE_CURVE('',#12404,#12405,#6949,.T.);
#15719=EDGE_CURVE('',#12405,#12406,#6950,.T.);
#15720=EDGE_CURVE('',#12406,#12407,#6951,.T.);
#15721=EDGE_CURVE('',#12407,#12408,#6952,.T.);
#15722=EDGE_CURVE('',#12408,#12403,#6953,.T.);
#15723=EDGE_CURVE('',#12399,#12408,#6954,.T.);
#15724=EDGE_CURVE('',#12398,#12403,#6955,.T.);
#15725=EDGE_CURVE('',#12400,#12407,#6956,.T.);
#15726=EDGE_CURVE('',#12401,#12406,#6957,.T.);
#15727=EDGE_CURVE('',#12402,#12405,#6958,.T.);
#15728=EDGE_CURVE('',#12397,#12404,#6959,.T.);
#15729=EDGE_CURVE('',#12409,#12409,#10355,.T.);
#15730=EDGE_CURVE('',#12410,#12410,#10356,.T.);
#15731=EDGE_CURVE('',#12410,#12409,#6960,.T.);
#15732=EDGE_CURVE('',#12410,#12394,#6961,.T.);
#22024=ORIENTED_EDGE('',*,*,#15705,.T.);
#22025=ORIENTED_EDGE('',*,*,#15706,.T.);
#22026=ORIENTED_EDGE('',*,*,#15705,.F.);
#22027=ORIENTED_EDGE('',*,*,#15707,.T.);
#22028=ORIENTED_EDGE('',*,*,#15708,.T.);
#22029=ORIENTED_EDGE('',*,*,#15707,.F.);
#22030=ORIENTED_EDGE('',*,*,#15708,.F.);
#22031=ORIENTED_EDGE('',*,*,#15709,.T.);
#22032=ORIENTED_EDGE('',*,*,#15710,.T.);
#22033=ORIENTED_EDGE('',*,*,#15709,.F.);
#22034=ORIENTED_EDGE('',*,*,#15710,.F.);
#22035=ORIENTED_EDGE('',*,*,#15711,.T.);
#22036=ORIENTED_EDGE('',*,*,#15712,.T.);
#22037=ORIENTED_EDGE('',*,*,#15713,.T.);
#22038=ORIENTED_EDGE('',*,*,#15714,.T.);
#22039=ORIENTED_EDGE('',*,*,#15715,.T.);
#22040=ORIENTED_EDGE('',*,*,#15716,.T.);
#22041=ORIENTED_EDGE('',*,*,#15717,.T.);
#22042=ORIENTED_EDGE('',*,*,#15718,.T.);
#22043=ORIENTED_EDGE('',*,*,#15719,.T.);
#22044=ORIENTED_EDGE('',*,*,#15720,.T.);
#22045=ORIENTED_EDGE('',*,*,#15721,.T.);
#22046=ORIENTED_EDGE('',*,*,#15722,.T.);
#22047=ORIENTED_EDGE('',*,*,#15722,.F.);
#22048=ORIENTED_EDGE('',*,*,#15723,.F.);
#22049=ORIENTED_EDGE('',*,*,#15712,.F.);
#22050=ORIENTED_EDGE('',*,*,#15724,.T.);
#22051=ORIENTED_EDGE('',*,*,#15721,.F.);
#22052=ORIENTED_EDGE('',*,*,#15725,.F.);
#22053=ORIENTED_EDGE('',*,*,#15713,.F.);
#22054=ORIENTED_EDGE('',*,*,#15723,.T.);
#22055=ORIENTED_EDGE('',*,*,#15720,.F.);
#22056=ORIENTED_EDGE('',*,*,#15726,.F.);
#22057=ORIENTED_EDGE('',*,*,#15714,.F.);
#22058=ORIENTED_EDGE('',*,*,#15725,.T.);
#22059=ORIENTED_EDGE('',*,*,#15719,.F.);
#22060=ORIENTED_EDGE('',*,*,#15727,.F.);
#22061=ORIENTED_EDGE('',*,*,#15715,.F.);
#22062=ORIENTED_EDGE('',*,*,#15726,.T.);
#22063=ORIENTED_EDGE('',*,*,#15718,.F.);
#22064=ORIENTED_EDGE('',*,*,#15728,.F.);
#22065=ORIENTED_EDGE('',*,*,#15716,.F.);
#22066=ORIENTED_EDGE('',*,*,#15727,.T.);
#22067=ORIENTED_EDGE('',*,*,#15717,.F.);
#22068=ORIENTED_EDGE('',*,*,#15724,.F.);
#22069=ORIENTED_EDGE('',*,*,#15711,.F.);
#22070=ORIENTED_EDGE('',*,*,#15728,.T.);
#22071=ORIENTED_EDGE('',*,*,#15729,.T.);
#22072=ORIENTED_EDGE('',*,*,#15730,.T.);
#22073=ORIENTED_EDGE('',*,*,#15731,.T.);
#22074=ORIENTED_EDGE('',*,*,#15729,.F.);
#22075=ORIENTED_EDGE('',*,*,#15731,.F.);
#22076=ORIENTED_EDGE('',*,*,#15730,.F.);
#22077=ORIENTED_EDGE('',*,*,#15732,.T.);
#22078=ORIENTED_EDGE('',*,*,#15706,.F.);
#22079=ORIENTED_EDGE('',*,*,#15732,.F.);
#24107=CYLINDRICAL_SURFACE('',#27983,5.);
#24108=CYLINDRICAL_SURFACE('',#28000,3.);
#25292=ADVANCED_FACE('',(#3339,#1406),#2045,.T.);
#25293=ADVANCED_FACE('',(#3340),#24107,.T.);
#25294=ADVANCED_FACE('',(#3341),#79,.T.);
#25295=ADVANCED_FACE('',(#3342,#1407),#2046,.T.);
#25296=ADVANCED_FACE('',(#3343),#2047,.F.);
#25297=ADVANCED_FACE('',(#3344),#2048,.F.);
#25298=ADVANCED_FACE('',(#3345),#2049,.F.);
#25299=ADVANCED_FACE('',(#3346),#2050,.F.);
#25300=ADVANCED_FACE('',(#3347),#2051,.F.);
#25301=ADVANCED_FACE('',(#3348),#2052,.F.);
#25302=ADVANCED_FACE('',(#3349),#2053,.F.);
#25303=ADVANCED_FACE('',(#3350),#2054,.T.);
#25304=ADVANCED_FACE('',(#3351),#552,.T.);
#25305=ADVANCED_FACE('',(#3352),#24108,.T.);
#25684=CLOSED_SHELL('',(#25292,#25293,#25294,#25295,#25296,#25297,#25298,
#25299,#25300,#25301,#25302,#25303,#25304,#25305));
#27979=AXIS2_PLACEMENT_3D('',#64122,#34090,#34091);
#27980=AXIS2_PLACEMENT_3D('',#64123,#34092,#34093);
#27981=AXIS2_PLACEMENT_3D('',#64125,#34094,#34095);
#27982=AXIS2_PLACEMENT_3D('',#64127,#34096,#34097);
#27983=AXIS2_PLACEMENT_3D('',#64128,#34098,#34099);
#27984=AXIS2_PLACEMENT_3D('',#64131,#34101,#34102);
#27985=AXIS2_PLACEMENT_3D('',#64132,#34103,#34104);
#27986=AXIS2_PLACEMENT_3D('',#64134,#34105,#34106);
#27987=AXIS2_PLACEMENT_3D('',#64135,#34107,#34108);
#27988=AXIS2_PLACEMENT_3D('',#64136,#34109,#34110);
#27989=AXIS2_PLACEMENT_3D('',#64149,#34117,#34118);
#27990=AXIS2_PLACEMENT_3D('',#64162,#34125,#34126);
#27991=AXIS2_PLACEMENT_3D('',#64165,#34129,#34130);
#27992=AXIS2_PLACEMENT_3D('',#64167,#34132,#34133);
#27993=AXIS2_PLACEMENT_3D('',#64169,#34135,#34136);
#27994=AXIS2_PLACEMENT_3D('',#64171,#34138,#34139);
#27995=AXIS2_PLACEMENT_3D('',#64173,#34141,#34142);
#27996=AXIS2_PLACEMENT_3D('',#64174,#34143,#34144);
#27997=AXIS2_PLACEMENT_3D('',#64176,#34145,#34146);
#27998=AXIS2_PLACEMENT_3D('',#64177,#34147,#34148);
#27999=AXIS2_PLACEMENT_3D('',#64179,#34149,#34150);
#28000=AXIS2_PLACEMENT_3D('',#64181,#34152,#34153);
#34090=DIRECTION('axis',(0.,0.,1.));
#34091=DIRECTION('refdir',(1.,0.,0.));
#34092=DIRECTION('center_axis',(0.,1.,0.));
#34093=DIRECTION('ref_axis',(1.,0.,0.));
#34094=DIRECTION('center_axis',(0.,1.,0.));
#34095=DIRECTION('ref_axis',(1.,0.,0.));
#34096=DIRECTION('center_axis',(0.,-1.,0.));
#34097=DIRECTION('ref_axis',(1.,0.,0.));
#34098=DIRECTION('center_axis',(0.,1.,0.));
#34099=DIRECTION('ref_axis',(1.,0.,0.));
#34100=DIRECTION('',(0.,-1.,0.));
#34101=DIRECTION('center_axis',(0.,1.,0.));
#34102=DIRECTION('ref_axis',(1.,0.,0.));
#34103=DIRECTION('center_axis',(0.,1.,0.));
#34104=DIRECTION('ref_axis',(1.,0.,0.));
#34105=DIRECTION('center_axis',(0.,0.,1.));
#34106=DIRECTION('ref_axis',(-1.,0.,0.));
#34107=DIRECTION('center_axis',(0.,1.,0.));
#34108=DIRECTION('ref_axis',(1.,0.,0.));
#34109=DIRECTION('center_axis',(2.27272746077357E-11,-1.,0.));
#34110=DIRECTION('ref_axis',(0.,0.,-1.));
#34111=DIRECTION('',(0.,0.,1.));
#34112=DIRECTION('',(0.866025403795548,1.96823971693366E-11,0.499999999980758));
#34113=DIRECTION('',(0.866025403795548,1.96823971693366E-11,-0.499999999980758));
#34114=DIRECTION('',(0.,0.,-1.));
#34115=DIRECTION('',(-0.866025403795548,-1.96823971693366E-11,-0.499999999980758));
#34116=DIRECTION('',(-0.866025403795548,-1.96823971693366E-11,0.499999999980758));
#34117=DIRECTION('center_axis',(0.,1.,0.));
#34118=DIRECTION('ref_axis',(1.,0.,0.));
#34119=DIRECTION('',(0.,0.,-1.));
#34120=DIRECTION('',(0.866025403795548,0.,-0.499999999980758));
#34121=DIRECTION('',(0.866025403795548,0.,0.499999999980758));
#34122=DIRECTION('',(0.,0.,1.));
#34123=DIRECTION('',(-0.866025403795548,0.,0.499999999980758));
#34124=DIRECTION('',(-0.866025403795548,0.,-0.499999999980758));
#34125=DIRECTION('center_axis',(-0.499999999980758,0.,0.866025403795548));
#34126=DIRECTION('ref_axis',(0.,1.,0.));
#34127=DIRECTION('',(0.,1.,0.));
#34128=DIRECTION('',(0.,1.,0.));
#34129=DIRECTION('center_axis',(0.499999999980758,0.,0.866025403795548));
#34130=DIRECTION('ref_axis',(0.,-1.,0.));
#34131=DIRECTION('',(0.,1.,0.));
#34132=DIRECTION('center_axis',(1.,0.,0.));
#34133=DIRECTION('ref_axis',(0.,1.,0.));
#34134=DIRECTION('',(0.,1.,0.));
#34135=DIRECTION('center_axis',(0.499999999980758,0.,-0.866025403795548));
#34136=DIRECTION('ref_axis',(0.,-1.,0.));
#34137=DIRECTION('',(0.,1.,0.));
#34138=DIRECTION('center_axis',(-0.499999999980758,0.,-0.866025403795548));
#34139=DIRECTION('ref_axis',(-0.866025403795548,0.,0.499999999980758));
#34140=DIRECTION('',(0.,1.,0.));
#34141=DIRECTION('center_axis',(-1.,0.,0.));
#34142=DIRECTION('ref_axis',(0.,0.,1.));
#34143=DIRECTION('center_axis',(0.,1.,0.));
#34144=DIRECTION('ref_axis',(1.,0.,0.));
#34145=DIRECTION('center_axis',(0.,1.,0.));
#34146=DIRECTION('ref_axis',(1.,0.,0.));
#34147=DIRECTION('center_axis',(0.,-1.,0.));
#34148=DIRECTION('ref_axis',(1.,0.,0.));
#34149=DIRECTION('center_axis',(0.,1.,0.));
#34150=DIRECTION('ref_axis',(1.,0.,0.));
#34151=DIRECTION('',(0.707106781186547,0.707106781186548,8.65956056235493E-17));
#34152=DIRECTION('center_axis',(0.,1.,0.));
#34153=DIRECTION('ref_axis',(1.,0.,0.));
#34154=DIRECTION('',(0.,-1.,0.));
#64122=CARTESIAN_POINT('',(0.,0.,0.));
#64123=CARTESIAN_POINT('Origin',(26.5,-12.,-20.));
#64124=CARTESIAN_POINT('',(19.,-12.,-20.));
#64125=CARTESIAN_POINT('Origin',(24.,-12.,-20.));
#64126=CARTESIAN_POINT('',(21.,-12.,-20.));
#64127=CARTESIAN_POINT('Origin',(24.,-12.,-20.));
#64128=CARTESIAN_POINT('Origin',(24.,-14.7,-20.));
#64129=CARTESIAN_POINT('',(19.,-17.4,-20.));
#64130=CARTESIAN_POINT('',(19.,-14.7,-20.));
#64131=CARTESIAN_POINT('Origin',(24.,-17.4,-20.));
#64132=CARTESIAN_POINT('Origin',(24.,-17.3999999999,-20.));
#64133=CARTESIAN_POINT('',(19.6,-17.9999999999,-20.));
#64134=CARTESIAN_POINT('Origin',(19.6000000001,-17.3999999999,-20.));
#64135=CARTESIAN_POINT('Origin',(24.,-17.9999999999,-20.));
#64136=CARTESIAN_POINT('Origin',(26.2,-17.99999999995,-20.));
#64137=CARTESIAN_POINT('',(21.5,-18.,-21.443375673));
#64138=CARTESIAN_POINT('',(21.5,-18.,-18.556624327));
#64139=CARTESIAN_POINT('',(21.5,-18.,-20.));
#64140=CARTESIAN_POINT('',(24.,-18.,-17.1132486541));
#64141=CARTESIAN_POINT('',(23.5750000000476,-18.,-17.3586225184655));
#64142=CARTESIAN_POINT('',(26.5,-18.,-18.556624327));
#64143=CARTESIAN_POINT('',(26.0749999999947,-18.,-18.3112504626039));
#64144=CARTESIAN_POINT('',(26.5,-18.,-21.443375673));
#64145=CARTESIAN_POINT('',(26.5,-18.,-19.63915608175));
#64146=CARTESIAN_POINT('',(24.,-18.,-22.8867513459));
#64147=CARTESIAN_POINT('',(26.0749999999947,-18.,-21.6887495373961));
#64148=CARTESIAN_POINT('',(23.5750000000476,-18.,-22.6413774815345));
#64149=CARTESIAN_POINT('Origin',(24.,-15.,-20.));
#64150=CARTESIAN_POINT('',(21.5,-15.,-18.556624327));
#64151=CARTESIAN_POINT('',(21.5,-15.,-21.443375673));
#64152=CARTESIAN_POINT('',(21.5,-15.,-21.443375673));
#64153=CARTESIAN_POINT('',(24.,-15.,-22.8867513459));
#64154=CARTESIAN_POINT('',(24.,-15.,-22.8867513459));
#64155=CARTESIAN_POINT('',(26.5,-15.,-21.443375673));
#64156=CARTESIAN_POINT('',(26.5,-15.,-21.443375673));
#64157=CARTESIAN_POINT('',(26.5,-15.,-18.556624327));
#64158=CARTESIAN_POINT('',(26.5,-15.,-20.));
#64159=CARTESIAN_POINT('',(24.,-15.,-17.1132486541));
#64160=CARTESIAN_POINT('',(24.,-15.,-17.1132486541));
#64161=CARTESIAN_POINT('',(21.5,-15.,-18.556624327));
#64162=CARTESIAN_POINT('Origin',(22.75,-18.,-17.83493649055));
#64163=CARTESIAN_POINT('',(24.,-18.,-17.1132486541));
#64164=CARTESIAN_POINT('',(21.5,-18.,-18.556624327));
#64165=CARTESIAN_POINT('Origin',(25.25,-18.,-17.83493649055));
#64166=CARTESIAN_POINT('',(26.5,-18.,-18.556624327));
#64167=CARTESIAN_POINT('Origin',(26.5,-18.,-19.2783121635));
#64168=CARTESIAN_POINT('',(26.5,-18.,-21.443375673));
#64169=CARTESIAN_POINT('Origin',(25.25,-18.,-22.16506350945));
#64170=CARTESIAN_POINT('',(24.,-18.,-22.8867513459));
#64171=CARTESIAN_POINT('Origin',(22.75,-18.,-22.16506350945));
#64172=CARTESIAN_POINT('',(21.5,-18.,-21.443375673));
#64173=CARTESIAN_POINT('Origin',(21.5,-18.,-20.));
#64174=CARTESIAN_POINT('Origin',(25.193275,8.,-20.));
#64175=CARTESIAN_POINT('',(21.61345,8.,-20.));
#64176=CARTESIAN_POINT('Origin',(24.,8.,-20.));
#64177=CARTESIAN_POINT('Origin',(24.,7.693275,-20.));
#64178=CARTESIAN_POINT('',(21.,7.38655,-20.));
#64179=CARTESIAN_POINT('Origin',(24.,7.38655,-20.));
#64180=CARTESIAN_POINT('',(21.306725,7.693275,-20.));
#64181=CARTESIAN_POINT('Origin',(24.,-2.306725,-20.));
#64182=CARTESIAN_POINT('',(21.,-2.306725,-20.));
#66669=UNCERTAINTY_MEASURE_WITH_UNIT(LENGTH_MEASURE(0.01),#66722,
'DISTANCE_ACCURACY_VALUE',
'Maximum model space distance between geometric entities at asserted c
onnectivities');
#66680=UNCERTAINTY_MEASURE_WITH_UNIT(LENGTH_MEASURE(0.01),#66722,
'DISTANCE_ACCURACY_VALUE',
'Maximum model space distance between geometric entities at asserted c
onnectivities');
#66710=(
GEOMETRIC_REPRESENTATION_CONTEXT(3)
GLOBAL_UNCERTAINTY_ASSIGNED_CONTEXT((#66669))
GLOBAL_UNIT_ASSIGNED_CONTEXT((#66722,#66724,#66725))
REPRESENTATION_CONTEXT('','3D')
);
#66721=(
GEOMETRIC_REPRESENTATION_CONTEXT(3)
GLOBAL_UNCERTAINTY_ASSIGNED_CONTEXT((#66680))
GLOBAL_UNIT_ASSIGNED_CONTEXT((#66722,#66724,#66725))
REPRESENTATION_CONTEXT('','3D')
);
#66722=(
LENGTH_UNIT()
NAMED_UNIT(*)
SI_UNIT(.MILLI.,.METRE.)
);
#66724=(
NAMED_UNIT(*)
PLANE_ANGLE_UNIT()
SI_UNIT($,.RADIAN.)
);
#66725=(
NAMED_UNIT(*)
SI_UNIT($,.STERADIAN.)
SOLID_ANGLE_UNIT()
);
#66755=SHAPE_DEFINITION_REPRESENTATION(#66815,#66919);
#66815=PRODUCT_DEFINITION_SHAPE('',$,#66960);
#66919=SHAPE_REPRESENTATION('',(#27979),#66710);
#66930=PRODUCT_DEFINITION_CONTEXT('part definition',#67052,'design');
#66960=PRODUCT_DEFINITION('Coupling Clamp Screw 2',
'Coupling Clamp Screw 2',#67000,#66930);
#67000=PRODUCT_DEFINITION_FORMATION('',$,#67083);
#67052=APPLICATION_CONTEXT(
'Core Data for Automotive Mechanical Design Process');
#67053=PRODUCT_CONTEXT('part definition',#67052,'mechanical');
#67083=PRODUCT('Coupling Clamp Screw 2','Coupling Clamp Screw 2',$,(#67053));
#67095=PRESENTATION_STYLE_ASSIGNMENT((#67097));
#67097=SURFACE_STYLE_USAGE(.BOTH.,#67099);
#67099=SURFACE_SIDE_STYLE('',(#67101));
#67101=SURFACE_STYLE_FILL_AREA(#67103);
#67103=FILL_AREA_STYLE('Opaque(202,209,238)',(#67105));
#67105=FILL_AREA_STYLE_COLOUR('Opaque(202,209,238)',#67107);
#67107=COLOUR_RGB('Opaque(202,209,238)',0.792156862745098,0.819607843137255,
0.933333333333333);
ENDSEC;
END-ISO-10303-21;
